ISO-10303-21;
HEADER;
/* Generated by software containing ST-Developer
 * from STEP Tools, Inc. (www.steptools.com) 
 */

FILE_DESCRIPTION(
/* description */ ('Bin tilter linkage'),
/* implementation_level */ '2;1');

FILE_NAME(
/* name */ 'M4 short cap screw (7).step',
/* time_stamp */ '2026-10-28T03:26:24-07:00',
/* author */ (''),
/* organization */ (''),
/* preprocessor_version */ 'ST-DEVELOPER v20.2',
/* originating_system */ 'Autodesk Translation Framework v15.17.0.0',
/* authorisation */ '');

FILE_SCHEMA (('AUTOMOTIVE_DESIGN { 1 0 10303 214 3 1 1 }'));
ENDSEC;

DATA;
#10=MECHANICAL_DESIGN_GEOMETRIC_PRESENTATION_REPRESENTATION('',(#902),#23728);
#690=SHAPE_REPRESENTATION_RELATIONSHIP('SRR','None',#24155,#796);
#796=ADVANCED_BREP_SHAPE_REPRESENTATION('',(#1015),#23655);
#902=STYLED_ITEM('',(#24772),#1015);
#1015=MANIFOLD_SOLID_BREP('Body1',#12433);
#1281=FACE_BOUND('',#3178,.T.);
#1646=PLANE('',#14356);
#1647=PLANE('',#14361);
#1648=PLANE('',#14364);
#2206=FACE_OUTER_BOUND('',#3177,.T.);
#2207=FACE_OUTER_BOUND('',#3179,.T.);
#2208=FACE_OUTER_BOUND('',#3180,.T.);
#2209=FACE_OUTER_BOUND('',#3181,.T.);
#2210=FACE_OUTER_BOUND('',#3182,.T.);
#3177=EDGE_LOOP('',(#9613));
#3178=EDGE_LOOP('',(#9614));
#3179=EDGE_LOOP('',(#9615,#9616,#9617,#9618));
#3180=EDGE_LOOP('',(#9619));
#3181=EDGE_LOOP('',(#9620,#9621,#9622,#9623));
#3182=EDGE_LOOP('',(#9624));
#4149=LINE('',#21145,#4824);
#4150=LINE('',#21149,#4825);
#4824=VECTOR('',#17144,0.35);
#4825=VECTOR('',#17149,0.2);
#5519=CIRCLE('',#14357,0.35);
#5520=CIRCLE('',#14358,0.2);
#5521=CIRCLE('',#14360,0.35);
#5522=CIRCLE('',#14363,0.2);
#6369=VERTEX_POINT('',#21138);
#6370=VERTEX_POINT('',#21140);
#6371=VERTEX_POINT('',#21143);
#6372=VERTEX_POINT('',#21148);
#7546=EDGE_CURVE('',#6369,#6369,#5519,.T.);
#7547=EDGE_CURVE('',#6370,#6370,#5520,.T.);
#7548=EDGE_CURVE('',#6371,#6371,#5521,.T.);
#7549=EDGE_CURVE('',#6371,#6369,#4149,.T.);
#7550=EDGE_CURVE('',#6370,#6372,#4150,.T.);
#7551=EDGE_CURVE('',#6372,#6372,#5522,.T.);
#9613=ORIENTED_EDGE('',*,*,#7546,.F.);
#9614=ORIENTED_EDGE('',*,*,#7547,.T.);
#9615=ORIENTED_EDGE('',*,*,#7548,.F.);
#9616=ORIENTED_EDGE('',*,*,#7549,.T.);
#9617=ORIENTED_EDGE('',*,*,#7546,.T.);
#9618=ORIENTED_EDGE('',*,*,#7549,.F.);
#9619=ORIENTED_EDGE('',*,*,#7548,.T.);
#9620=ORIENTED_EDGE('',*,*,#7547,.F.);
#9621=ORIENTED_EDGE('',*,*,#7550,.T.);
#9622=ORIENTED_EDGE('',*,*,#7551,.T.);
#9623=ORIENTED_EDGE('',*,*,#7550,.F.);
#9624=ORIENTED_EDGE('',*,*,#7551,.F.);
#11425=CYLINDRICAL_SURFACE('',#14359,0.35);
#11426=CYLINDRICAL_SURFACE('',#14362,0.2);
#11931=ADVANCED_FACE('',(#2206,#1281),#1646,.F.);
#11932=ADVANCED_FACE('',(#2207),#11425,.T.);
#11933=ADVANCED_FACE('',(#2208),#1647,.T.);
#11934=ADVANCED_FACE('',(#2209),#11426,.T.);
#11935=ADVANCED_FACE('',(#2210),#1648,.F.);
#12433=CLOSED_SHELL('',(#11931,#11932,#11933,#11934,#11935));
#14355=AXIS2_PLACEMENT_3D('',#21136,#17132,#17133);
#14356=AXIS2_PLACEMENT_3D('',#21137,#17134,#17135);
#14357=AXIS2_PLACEMENT_3D('',#21139,#17136,#17137);
#14358=AXIS2_PLACEMENT_3D('',#21141,#17138,#17139);
#14359=AXIS2_PLACEMENT_3D('',#21142,#17140,#17141);
#14360=AXIS2_PLACEMENT_3D('',#21144,#17142,#17143);
#14361=AXIS2_PLACEMENT_3D('',#21146,#17145,#17146);
#14362=AXIS2_PLACEMENT_3D('',#21147,#17147,#17148);
#14363=AXIS2_PLACEMENT_3D('',#21150,#17150,#17151);
#14364=AXIS2_PLACEMENT_3D('',#21151,#17152,#17153);
#17132=DIRECTION('axis',(0.,0.,1.));
#17133=DIRECTION('refdir',(1.,0.,0.));
#17134=DIRECTION('center_axis',(0.,1.,0.));
#17135=DIRECTION('ref_axis',(1.,0.,0.));
#17136=DIRECTION('center_axis',(0.,1.,0.));
#17137=DIRECTION('ref_axis',(1.,0.,0.));
#17138=DIRECTION('center_axis',(0.,1.,0.));
#17139=DIRECTION('ref_axis',(1.,0.,0.));
#17140=DIRECTION('center_axis',(0.,1.,0.));
#17141=DIRECTION('ref_axis',(1.,0.,0.));
#17142=DIRECTION('center_axis',(0.,1.,0.));
#17143=DIRECTION('ref_axis',(1.,0.,0.));
#17144=DIRECTION('',(0.,-1.,0.));
#17145=DIRECTION('center_axis',(0.,1.,0.));
#17146=DIRECTION('ref_axis',(1.,0.,0.));
#17147=DIRECTION('center_axis',(0.,1.,0.));
#17148=DIRECTION('ref_axis',(1.,0.,0.));
#17149=DIRECTION('',(0.,-1.,0.));
#17150=DIRECTION('center_axis',(0.,1.,0.));
#17151=DIRECTION('ref_axis',(1.,0.,0.));
#17152=DIRECTION('center_axis',(0.,1.,0.));
#17153=DIRECTION('ref_axis',(1.,0.,0.));
#21136=CARTESIAN_POINT('',(0.,0.,0.));
#21137=CARTESIAN_POINT('Origin',(1.30814754519511,0.8,13.6918524548049));
#21138=CARTESIAN_POINT('',(0.958147545195112,0.8,13.6918524548049));
#21139=CARTESIAN_POINT('Origin',(1.30814754519511,0.8,13.6918524548049));
#21140=CARTESIAN_POINT('',(1.10814754519511,0.8,13.6918524548049));
#21141=CARTESIAN_POINT('Origin',(1.30814754519511,0.8,13.6918524548049));
#21142=CARTESIAN_POINT('Origin',(1.30814754519511,0.8,13.6918524548049));
#21143=CARTESIAN_POINT('',(0.958147545195112,1.2,13.6918524548049));
#21144=CARTESIAN_POINT('Origin',(1.30814754519511,1.2,13.6918524548049));
#21145=CARTESIAN_POINT('',(0.958147545195112,0.8,13.6918524548049));
#21146=CARTESIAN_POINT('Origin',(1.30814754519511,1.2,13.6918524548049));
#21147=CARTESIAN_POINT('Origin',(1.30814754519511,0.1,13.6918524548049));
#21148=CARTESIAN_POINT('',(1.10814754519511,0.1,13.6918524548049));
#21149=CARTESIAN_POINT('',(1.10814754519511,0.1,13.6918524548049));
#21150=CARTESIAN_POINT('Origin',(1.30814754519511,0.1,13.6918524548049));
#21151=CARTESIAN_POINT('Origin',(1.30814754519511,0.1,13.6918524548049));
#23538=UNCERTAINTY_MEASURE_WITH_UNIT(LENGTH_MEASURE(0.001),#23729,
'DISTANCE_ACCURACY_VALUE',
'Maximum model space distance between geometric entities at asserted c
onnectivities');
#23611=UNCERTAINTY_MEASURE_WITH_UNIT(LENGTH_MEASURE(0.001),#23729,
'DISTANCE_ACCURACY_VALUE',
'Maximum model space distance between geometric entities at asserted c
onnectivities');
#23655=(
GEOMETRIC_REPRESENTATION_CONTEXT(3)
GLOBAL_UNCERTAINTY_ASSIGNED_CONTEXT((#23538))
GLOBAL_UNIT_ASSIGNED_CONTEXT((#23729,#23731,#23732))
REPRESENTATION_CONTEXT('','3D')
);
#23728=(
GEOMETRIC_REPRESENTATION_CONTEXT(3)
GLOBAL_UNCERTAINTY_ASSIGNED_CONTEXT((#23611))
GLOBAL_UNIT_ASSIGNED_CONTEXT((#23729,#23731,#23732))
REPRESENTATION_CONTEXT('','3D')
);
#23729=(
LENGTH_UNIT()
NAMED_UNIT(*)
SI_UNIT(.CENTI.,.METRE.)
);
#23731=(
NAMED_UNIT(*)
PLANE_ANGLE_UNIT()
SI_UNIT($,.RADIAN.)
);
#23732=(
NAMED_UNIT(*)
SI_UNIT($,.STERADIAN.)
SOLID_ANGLE_UNIT()
);
#23776=SHAPE_DEFINITION_REPRESENTATION(#23892,#24155);
#23892=PRODUCT_DEFINITION_SHAPE('',$,#24272);
#24155=SHAPE_REPRESENTATION('',(#14355),#23655);
#24228=PRODUCT_DEFINITION_CONTEXT('part definition',#24578,'design');
#24272=PRODUCT_DEFINITION('M4 short cap screw (7)',
'M4 short cap screw (7)',#24388,#24228);
#24388=PRODUCT_DEFINITION_FORMATION('',$,#24623);
#24578=APPLICATION_CONTEXT(
'Core Data for Automotive Mechanical Design Process');
#24579=PRODUCT_CONTEXT('part definition',#24578,'mechanical');
#24623=PRODUCT('M4 short cap screw (7)','M4 short cap screw (7)',
'M4 short cap screw (7)',(#24579));
#24766=COLOUR_RGB('Black',0.12,0.14,0.17);
#24767=FILL_AREA_STYLE_COLOUR('',#24766);
#24768=FILL_AREA_STYLE('',(#24767));
#24769=SURFACE_STYLE_FILL_AREA(#24768);
#24770=SURFACE_SIDE_STYLE('',(#24769));
#24771=SURFACE_STYLE_USAGE(.BOTH.,#24770);
#24772=PRESENTATION_STYLE_ASSIGNMENT((#24771));
ENDSEC;
END-ISO-10303-21;
